ISO-10303-21;
HEADER;
/* Generated by software containing ST-Developer
 * from STEP Tools, Inc. (www.steptools.com) 
 */

FILE_DESCRIPTION(
/* description */ ('PAT-097'),
/* implementation_level */ '2;1');

FILE_NAME(
/* name */ 'M8 captive slot nut.step',
/* time_stamp */ '2026-10-29T15:59:31-07:00',
/* author */ (''),
/* organization */ (''),
/* preprocessor_version */ 'ST-DEVELOPER v20.2',
/* originating_system */ 'Autodesk Translation Framework v15.17.0.0',
/* authorisation */ '');

FILE_SCHEMA (('AUTOMOTIVE_DESIGN { 1 0 10303 214 3 1 1 }'));
ENDSEC;

DATA;
#10=MECHANICAL_DESIGN_GEOMETRIC_PRESENTATION_REPRESENTATION('',(#76),#2768);
#62=SHAPE_REPRESENTATION_RELATIONSHIP('SRR','None',#2800,#69);
#69=ADVANCED_BREP_SHAPE_REPRESENTATION('',(#83),#2762);
#76=STYLED_ITEM('',(#2918),#83);
#83=MANIFOLD_SOLID_BREP('Body1',#1597);
#109=CYLINDRICAL_SURFACE('',#1758,0.34);
#156=FACE_BOUND('',#381,.T.);
#157=FACE_BOUND('',#389,.T.);
#204=CIRCLE('',#1759,0.34);
#205=CIRCLE('',#1760,0.34);
#254=FACE_OUTER_BOUND('',#377,.T.);
#255=FACE_OUTER_BOUND('',#378,.T.);
#256=FACE_OUTER_BOUND('',#379,.T.);
#257=FACE_OUTER_BOUND('',#380,.T.);
#258=FACE_OUTER_BOUND('',#382,.T.);
#259=FACE_OUTER_BOUND('',#383,.T.);
#260=FACE_OUTER_BOUND('',#384,.T.);
#261=FACE_OUTER_BOUND('',#385,.T.);
#262=FACE_OUTER_BOUND('',#386,.T.);
#263=FACE_OUTER_BOUND('',#387,.T.);
#264=FACE_OUTER_BOUND('',#388,.T.);
#377=EDGE_LOOP('',(#1241,#1242,#1243,#1244));
#378=EDGE_LOOP('',(#1245,#1246,#1247,#1248));
#379=EDGE_LOOP('',(#1249,#1250,#1251,#1252));
#380=EDGE_LOOP('',(#1253,#1254,#1255,#1256));
#381=EDGE_LOOP('',(#1257));
#382=EDGE_LOOP('',(#1258,#1259,#1260,#1261));
#383=EDGE_LOOP('',(#1262,#1263,#1264,#1265));
#384=EDGE_LOOP('',(#1266,#1267,#1268,#1269));
#385=EDGE_LOOP('',(#1270,#1271,#1272,#1273,#1274,#1275,#1276,#1277));
#386=EDGE_LOOP('',(#1278,#1279,#1280,#1281));
#387=EDGE_LOOP('',(#1282,#1283,#1284,#1285,#1286,#1287,#1288,#1289));
#388=EDGE_LOOP('',(#1290,#1291,#1292,#1293));
#389=EDGE_LOOP('',(#1294));
#490=LINE('',#2487,#627);
#491=LINE('',#2492,#628);
#492=LINE('',#2494,#629);
#493=LINE('',#2496,#630);
#494=LINE('',#2497,#631);
#495=LINE('',#2501,#632);
#496=LINE('',#2503,#633);
#497=LINE('',#2505,#634);
#498=LINE('',#2506,#635);
#499=LINE('',#2508,#636);
#500=LINE('',#2509,#637);
#501=LINE('',#2512,#638);
#502=LINE('',#2514,#639);
#503=LINE('',#2515,#640);
#504=LINE('',#2518,#641);
#505=LINE('',#2520,#642);
#506=LINE('',#2521,#643);
#507=LINE('',#2525,#644);
#508=LINE('',#2526,#645);
#509=LINE('',#2527,#646);
#510=LINE('',#2530,#647);
#511=LINE('',#2531,#648);
#512=LINE('',#2534,#649);
#513=LINE('',#2535,#650);
#514=LINE('',#2537,#651);
#627=VECTOR('',#2051,0.34);
#628=VECTOR('',#2056,1.);
#629=VECTOR('',#2057,1.);
#630=VECTOR('',#2058,1.);
#631=VECTOR('',#2059,1.);
#632=VECTOR('',#2062,1.);
#633=VECTOR('',#2063,1.);
#634=VECTOR('',#2064,1.);
#635=VECTOR('',#2065,1.);
#636=VECTOR('',#2068,1.);
#637=VECTOR('',#2069,1.);
#638=VECTOR('',#2072,1.);
#639=VECTOR('',#2073,1.);
#640=VECTOR('',#2074,1.);
#641=VECTOR('',#2077,1.);
#642=VECTOR('',#2078,1.);
#643=VECTOR('',#2079,1.);
#644=VECTOR('',#2082,1.);
#645=VECTOR('',#2083,1.);
#646=VECTOR('',#2084,1.);
#647=VECTOR('',#2087,1.);
#648=VECTOR('',#2088,1.);
#649=VECTOR('',#2091,1.);
#650=VECTOR('',#2092,1.);
#651=VECTOR('',#2095,1.);
#772=VERTEX_POINT('',#2484);
#773=VERTEX_POINT('',#2486);
#774=VERTEX_POINT('',#2490);
#775=VERTEX_POINT('',#2491);
#776=VERTEX_POINT('',#2493);
#777=VERTEX_POINT('',#2495);
#778=VERTEX_POINT('',#2499);
#779=VERTEX_POINT('',#2500);
#780=VERTEX_POINT('',#2502);
#781=VERTEX_POINT('',#2504);
#782=VERTEX_POINT('',#2511);
#783=VERTEX_POINT('',#2513);
#784=VERTEX_POINT('',#2517);
#785=VERTEX_POINT('',#2519);
#786=VERTEX_POINT('',#2523);
#787=VERTEX_POINT('',#2524);
#788=VERTEX_POINT('',#2529);
#789=VERTEX_POINT('',#2533);
#940=EDGE_CURVE('',#772,#772,#204,.T.);
#941=EDGE_CURVE('',#772,#773,#490,.T.);
#942=EDGE_CURVE('',#773,#773,#205,.T.);
#943=EDGE_CURVE('',#774,#775,#491,.T.);
#944=EDGE_CURVE('',#774,#776,#492,.T.);
#945=EDGE_CURVE('',#777,#776,#493,.T.);
#946=EDGE_CURVE('',#775,#777,#494,.T.);
#947=EDGE_CURVE('',#778,#779,#495,.T.);
#948=EDGE_CURVE('',#778,#780,#496,.T.);
#949=EDGE_CURVE('',#781,#780,#497,.T.);
#950=EDGE_CURVE('',#779,#781,#498,.T.);
#951=EDGE_CURVE('',#776,#781,#499,.T.);
#952=EDGE_CURVE('',#780,#777,#500,.T.);
#953=EDGE_CURVE('',#775,#782,#501,.T.);
#954=EDGE_CURVE('',#782,#783,#502,.T.);
#955=EDGE_CURVE('',#783,#774,#503,.T.);
#956=EDGE_CURVE('',#779,#784,#504,.T.);
#957=EDGE_CURVE('',#784,#785,#505,.T.);
#958=EDGE_CURVE('',#785,#778,#506,.T.);
#959=EDGE_CURVE('',#786,#787,#507,.T.);
#960=EDGE_CURVE('',#787,#783,#508,.T.);
#961=EDGE_CURVE('',#786,#782,#509,.T.);
#962=EDGE_CURVE('',#788,#786,#510,.T.);
#963=EDGE_CURVE('',#788,#785,#511,.T.);
#964=EDGE_CURVE('',#789,#788,#512,.T.);
#965=EDGE_CURVE('',#789,#784,#513,.T.);
#966=EDGE_CURVE('',#787,#789,#514,.T.);
#1241=ORIENTED_EDGE('',*,*,#940,.F.);
#1242=ORIENTED_EDGE('',*,*,#941,.T.);
#1243=ORIENTED_EDGE('',*,*,#942,.F.);
#1244=ORIENTED_EDGE('',*,*,#941,.F.);
#1245=ORIENTED_EDGE('',*,*,#943,.F.);
#1246=ORIENTED_EDGE('',*,*,#944,.T.);
#1247=ORIENTED_EDGE('',*,*,#945,.F.);
#1248=ORIENTED_EDGE('',*,*,#946,.F.);
#1249=ORIENTED_EDGE('',*,*,#947,.F.);
#1250=ORIENTED_EDGE('',*,*,#948,.T.);
#1251=ORIENTED_EDGE('',*,*,#949,.F.);
#1252=ORIENTED_EDGE('',*,*,#950,.F.);
#1253=ORIENTED_EDGE('',*,*,#951,.T.);
#1254=ORIENTED_EDGE('',*,*,#949,.T.);
#1255=ORIENTED_EDGE('',*,*,#952,.T.);
#1256=ORIENTED_EDGE('',*,*,#945,.T.);
#1257=ORIENTED_EDGE('',*,*,#942,.T.);
#1258=ORIENTED_EDGE('',*,*,#943,.T.);
#1259=ORIENTED_EDGE('',*,*,#953,.T.);
#1260=ORIENTED_EDGE('',*,*,#954,.T.);
#1261=ORIENTED_EDGE('',*,*,#955,.T.);
#1262=ORIENTED_EDGE('',*,*,#947,.T.);
#1263=ORIENTED_EDGE('',*,*,#956,.T.);
#1264=ORIENTED_EDGE('',*,*,#957,.T.);
#1265=ORIENTED_EDGE('',*,*,#958,.T.);
#1266=ORIENTED_EDGE('',*,*,#959,.T.);
#1267=ORIENTED_EDGE('',*,*,#960,.T.);
#1268=ORIENTED_EDGE('',*,*,#954,.F.);
#1269=ORIENTED_EDGE('',*,*,#961,.F.);
#1270=ORIENTED_EDGE('',*,*,#962,.T.);
#1271=ORIENTED_EDGE('',*,*,#961,.T.);
#1272=ORIENTED_EDGE('',*,*,#953,.F.);
#1273=ORIENTED_EDGE('',*,*,#946,.T.);
#1274=ORIENTED_EDGE('',*,*,#952,.F.);
#1275=ORIENTED_EDGE('',*,*,#948,.F.);
#1276=ORIENTED_EDGE('',*,*,#958,.F.);
#1277=ORIENTED_EDGE('',*,*,#963,.F.);
#1278=ORIENTED_EDGE('',*,*,#964,.T.);
#1279=ORIENTED_EDGE('',*,*,#963,.T.);
#1280=ORIENTED_EDGE('',*,*,#957,.F.);
#1281=ORIENTED_EDGE('',*,*,#965,.F.);
#1282=ORIENTED_EDGE('',*,*,#966,.T.);
#1283=ORIENTED_EDGE('',*,*,#965,.T.);
#1284=ORIENTED_EDGE('',*,*,#956,.F.);
#1285=ORIENTED_EDGE('',*,*,#950,.T.);
#1286=ORIENTED_EDGE('',*,*,#951,.F.);
#1287=ORIENTED_EDGE('',*,*,#944,.F.);
#1288=ORIENTED_EDGE('',*,*,#955,.F.);
#1289=ORIENTED_EDGE('',*,*,#960,.F.);
#1290=ORIENTED_EDGE('',*,*,#966,.F.);
#1291=ORIENTED_EDGE('',*,*,#959,.F.);
#1292=ORIENTED_EDGE('',*,*,#962,.F.);
#1293=ORIENTED_EDGE('',*,*,#964,.F.);
#1294=ORIENTED_EDGE('',*,*,#940,.T.);
#1473=PLANE('',#1761);
#1474=PLANE('',#1762);
#1475=PLANE('',#1763);
#1476=PLANE('',#1764);
#1477=PLANE('',#1765);
#1478=PLANE('',#1766);
#1479=PLANE('',#1767);
#1480=PLANE('',#1768);
#1481=PLANE('',#1769);
#1482=PLANE('',#1770);
#1547=ADVANCED_FACE('',(#254),#109,.F.);
#1548=ADVANCED_FACE('',(#255),#1473,.T.);
#1549=ADVANCED_FACE('',(#256),#1474,.T.);
#1550=ADVANCED_FACE('',(#257,#156),#1475,.T.);
#1551=ADVANCED_FACE('',(#258),#1476,.T.);
#1552=ADVANCED_FACE('',(#259),#1477,.T.);
#1553=ADVANCED_FACE('',(#260),#1478,.T.);
#1554=ADVANCED_FACE('',(#261),#1479,.T.);
#1555=ADVANCED_FACE('',(#262),#1480,.T.);
#1556=ADVANCED_FACE('',(#263),#1481,.T.);
#1557=ADVANCED_FACE('',(#264,#157),#1482,.F.);
#1597=CLOSED_SHELL('',(#1547,#1548,#1549,#1550,#1551,#1552,#1553,#1554,
#1555,#1556,#1557));
#1757=AXIS2_PLACEMENT_3D('',#2482,#2045,#2046);
#1758=AXIS2_PLACEMENT_3D('',#2483,#2047,#2048);
#1759=AXIS2_PLACEMENT_3D('',#2485,#2049,#2050);
#1760=AXIS2_PLACEMENT_3D('',#2488,#2052,#2053);
#1761=AXIS2_PLACEMENT_3D('',#2489,#2054,#2055);
#1762=AXIS2_PLACEMENT_3D('',#2498,#2060,#2061);
#1763=AXIS2_PLACEMENT_3D('',#2507,#2066,#2067);
#1764=AXIS2_PLACEMENT_3D('',#2510,#2070,#2071);
#1765=AXIS2_PLACEMENT_3D('',#2516,#2075,#2076);
#1766=AXIS2_PLACEMENT_3D('',#2522,#2080,#2081);
#1767=AXIS2_PLACEMENT_3D('',#2528,#2085,#2086);
#1768=AXIS2_PLACEMENT_3D('',#2532,#2089,#2090);
#1769=AXIS2_PLACEMENT_3D('',#2536,#2093,#2094);
#1770=AXIS2_PLACEMENT_3D('',#2538,#2096,#2097);
#2045=DIRECTION('axis',(0.,0.,1.));
#2046=DIRECTION('refdir',(1.,0.,0.));
#2047=DIRECTION('center_axis',(0.,0.,1.));
#2048=DIRECTION('ref_axis',(1.,0.,0.));
#2049=DIRECTION('center_axis',(0.,0.,1.));
#2050=DIRECTION('ref_axis',(1.,0.,0.));
#2051=DIRECTION('',(0.,0.,1.));
#2052=DIRECTION('center_axis',(0.,0.,-1.));
#2053=DIRECTION('ref_axis',(1.,0.,0.));
#2054=DIRECTION('center_axis',(0.,1.,0.));
#2055=DIRECTION('ref_axis',(-1.,0.,0.));
#2056=DIRECTION('',(1.,0.,0.));
#2057=DIRECTION('',(0.,0.,1.));
#2058=DIRECTION('',(-1.,0.,0.));
#2059=DIRECTION('',(0.,0.,1.));
#2060=DIRECTION('center_axis',(0.,-1.,0.));
#2061=DIRECTION('ref_axis',(1.,0.,0.));
#2062=DIRECTION('',(-1.,0.,0.));
#2063=DIRECTION('',(0.,0.,1.));
#2064=DIRECTION('',(1.,0.,0.));
#2065=DIRECTION('',(0.,0.,1.));
#2066=DIRECTION('center_axis',(0.,0.,1.));
#2067=DIRECTION('ref_axis',(1.,0.,0.));
#2068=DIRECTION('',(0.,-1.,0.));
#2069=DIRECTION('',(0.,1.,0.));
#2070=DIRECTION('center_axis',(0.,0.,1.));
#2071=DIRECTION('ref_axis',(1.,0.,0.));
#2072=DIRECTION('',(0.,1.,0.));
#2073=DIRECTION('',(-1.,0.,0.));
#2074=DIRECTION('',(0.,-1.,0.));
#2075=DIRECTION('center_axis',(0.,0.,1.));
#2076=DIRECTION('ref_axis',(1.,0.,0.));
#2077=DIRECTION('',(0.,-1.,0.));
#2078=DIRECTION('',(1.,0.,0.));
#2079=DIRECTION('',(0.,1.,0.));
#2080=DIRECTION('center_axis',(0.,1.,0.));
#2081=DIRECTION('ref_axis',(-1.,0.,0.));
#2082=DIRECTION('',(-1.,0.,0.));
#2083=DIRECTION('',(0.,0.,1.));
#2084=DIRECTION('',(0.,0.,1.));
#2085=DIRECTION('center_axis',(1.,0.,0.));
#2086=DIRECTION('ref_axis',(0.,1.,0.));
#2087=DIRECTION('',(0.,1.,0.));
#2088=DIRECTION('',(0.,0.,1.));
#2089=DIRECTION('center_axis',(0.,-1.,0.));
#2090=DIRECTION('ref_axis',(1.,0.,0.));
#2091=DIRECTION('',(1.,0.,0.));
#2092=DIRECTION('',(0.,0.,1.));
#2093=DIRECTION('center_axis',(-1.,0.,0.));
#2094=DIRECTION('ref_axis',(0.,-1.,0.));
#2095=DIRECTION('',(0.,-1.,0.));
#2096=DIRECTION('center_axis',(0.,0.,1.));
#2097=DIRECTION('ref_axis',(1.,0.,0.));
#2482=CARTESIAN_POINT('',(0.,0.,0.));
#2483=CARTESIAN_POINT('Origin',(0.,0.,0.2));
#2484=CARTESIAN_POINT('',(-0.34,-4.163799117101E-17,0.3));
#2485=CARTESIAN_POINT('Origin',(0.,0.,0.3));
#2486=CARTESIAN_POINT('',(-0.34,4.163799117101E-17,1.4));
#2487=CARTESIAN_POINT('',(-0.34,-4.163799117101E-17,0.2));
#2488=CARTESIAN_POINT('Origin',(0.,0.,1.4));
#2489=CARTESIAN_POINT('Origin',(1.,0.45,0.9));
#2490=CARTESIAN_POINT('',(-1.,0.45,0.9));
#2491=CARTESIAN_POINT('',(1.,0.45,0.9));
#2492=CARTESIAN_POINT('',(0.5,0.45,0.9));
#2493=CARTESIAN_POINT('',(-1.,0.45,1.4));
#2494=CARTESIAN_POINT('',(-1.,0.45,0.9));
#2495=CARTESIAN_POINT('',(1.,0.45,1.4));
#2496=CARTESIAN_POINT('',(1.,0.45,1.4));
#2497=CARTESIAN_POINT('',(1.,0.45,0.9));
#2498=CARTESIAN_POINT('Origin',(-1.,-0.45,0.9));
#2499=CARTESIAN_POINT('',(1.,-0.45,0.9));
#2500=CARTESIAN_POINT('',(-1.,-0.45,0.9));
#2501=CARTESIAN_POINT('',(-0.5,-0.45,0.9));
#2502=CARTESIAN_POINT('',(1.,-0.45,1.4));
#2503=CARTESIAN_POINT('',(1.,-0.45,0.9));
#2504=CARTESIAN_POINT('',(-1.,-0.45,1.4));
#2505=CARTESIAN_POINT('',(-1.,-0.45,1.4));
#2506=CARTESIAN_POINT('',(-1.,-0.45,0.9));
#2507=CARTESIAN_POINT('Origin',(0.,0.,1.4));
#2508=CARTESIAN_POINT('',(-1.,0.45,1.4));
#2509=CARTESIAN_POINT('',(1.,-0.45,1.4));
#2510=CARTESIAN_POINT('Origin',(0.,0.,0.9));
#2511=CARTESIAN_POINT('',(1.,0.8,0.9));
#2512=CARTESIAN_POINT('',(1.,-0.8,0.9));
#2513=CARTESIAN_POINT('',(-1.,0.8,0.9));
#2514=CARTESIAN_POINT('',(1.,0.8,0.9));
#2515=CARTESIAN_POINT('',(-1.,0.8,0.9));
#2516=CARTESIAN_POINT('Origin',(0.,0.,0.9));
#2517=CARTESIAN_POINT('',(-1.,-0.8,0.9));
#2518=CARTESIAN_POINT('',(-1.,0.8,0.9));
#2519=CARTESIAN_POINT('',(1.,-0.8,0.9));
#2520=CARTESIAN_POINT('',(-1.,-0.8,0.9));
#2521=CARTESIAN_POINT('',(1.,-0.8,0.9));
#2522=CARTESIAN_POINT('Origin',(1.,0.8,0.3));
#2523=CARTESIAN_POINT('',(1.,0.8,0.3));
#2524=CARTESIAN_POINT('',(-1.,0.8,0.3));
#2525=CARTESIAN_POINT('',(1.,0.8,0.3));
#2526=CARTESIAN_POINT('',(-1.,0.8,0.3));
#2527=CARTESIAN_POINT('',(1.,0.8,0.3));
#2528=CARTESIAN_POINT('Origin',(1.,-0.8,0.3));
#2529=CARTESIAN_POINT('',(1.,-0.8,0.3));
#2530=CARTESIAN_POINT('',(1.,-0.8,0.3));
#2531=CARTESIAN_POINT('',(1.,-0.8,0.3));
#2532=CARTESIAN_POINT('Origin',(-1.,-0.8,0.3));
#2533=CARTESIAN_POINT('',(-1.,-0.8,0.3));
#2534=CARTESIAN_POINT('',(-1.,-0.8,0.3));
#2535=CARTESIAN_POINT('',(-1.,-0.8,0.3));
#2536=CARTESIAN_POINT('Origin',(-1.,0.8,0.3));
#2537=CARTESIAN_POINT('',(-1.,0.8,0.3));
#2538=CARTESIAN_POINT('Origin',(0.,0.,0.3));
#2753=UNCERTAINTY_MEASURE_WITH_UNIT(LENGTH_MEASURE(0.001),#2769,
'DISTANCE_ACCURACY_VALUE',
'Maximum model space distance between geometric entities at asserted c
onnectivities');
#2759=UNCERTAINTY_MEASURE_WITH_UNIT(LENGTH_MEASURE(0.001),#2769,
'DISTANCE_ACCURACY_VALUE',
'Maximum model space distance between geometric entities at asserted c
onnectivities');
#2762=(
GEOMETRIC_REPRESENTATION_CONTEXT(3)
GLOBAL_UNCERTAINTY_ASSIGNED_CONTEXT((#2753))
GLOBAL_UNIT_ASSIGNED_CONTEXT((#2769,#2771,#2772))
REPRESENTATION_CONTEXT('','3D')
);
#2768=(
GEOMETRIC_REPRESENTATION_CONTEXT(3)
GLOBAL_UNCERTAINTY_ASSIGNED_CONTEXT((#2759))
GLOBAL_UNIT_ASSIGNED_CONTEXT((#2769,#2771,#2772))
REPRESENTATION_CONTEXT('','3D')
);
#2769=(
LENGTH_UNIT()
NAMED_UNIT(*)
SI_UNIT(.CENTI.,.METRE.)
);
#2771=(
NAMED_UNIT(*)
PLANE_ANGLE_UNIT()
SI_UNIT($,.RADIAN.)
);
#2772=(
NAMED_UNIT(*)
SI_UNIT($,.STERADIAN.)
SOLID_ANGLE_UNIT()
);
#2775=SHAPE_DEFINITION_REPRESENTATION(#2783,#2800);
#2783=PRODUCT_DEFINITION_SHAPE('',$,#2809);
#2800=SHAPE_REPRESENTATION('',(#1757),#2762);
#2806=PRODUCT_DEFINITION_CONTEXT('part definition',#2832,'design');
#2809=PRODUCT_DEFINITION('M8 captive slot nut',
'M8 captive slot nut',#2817,#2806);
#2817=PRODUCT_DEFINITION_FORMATION('',$,#2836);
#2832=APPLICATION_CONTEXT(
'Core Data for Automotive Mechanical Design Process');
#2833=PRODUCT_CONTEXT('part definition',#2832,'mechanical');
#2836=PRODUCT('M8 captive slot nut','M8 captive slot nut',
'M8 captive slot nut',(#2833));
#2912=COLOUR_RGB('Black',0.12,0.14,0.17);
#2913=FILL_AREA_STYLE_COLOUR('',#2912);
#2914=FILL_AREA_STYLE('',(#2913));
#2915=SURFACE_STYLE_FILL_AREA(#2914);
#2916=SURFACE_SIDE_STYLE('',(#2915));
#2917=SURFACE_STYLE_USAGE(.BOTH.,#2916);
#2918=PRESENTATION_STYLE_ASSIGNMENT((#2917));
ENDSEC;
END-ISO-10303-21;
